ISO-10303-21;
HEADER;
/* Generated by software containing ST-Developer
 * from STEP Tools, Inc. (www.steptools.com) 
 */

FILE_DESCRIPTION(
/* description */ (''),
/* implementation_level */ '2;1');

FILE_NAME(
/* name */ 'Pivot thrust washer.step',
/* time_stamp */ '2026-11-10T09:14:46-08:00',
/* author */ (''),
/* organization */ (''),
/* preprocessor_version */ 'ST-DEVELOPER v20.2',
/* originating_system */ 'Autodesk Translation Framework v15.17.0.0',
/* authorisation */ '');

FILE_SCHEMA (('AUTOMOTIVE_DESIGN { 1 0 10303 214 3 1 1 }'));
ENDSEC;

DATA;
#10=MECHANICAL_DESIGN_GEOMETRIC_PRESENTATION_REPRESENTATION('',(#567),#19471);
#547=SHAPE_REPRESENTATION_RELATIONSHIP('SRR','None',#19527,#557);
#557=ADVANCED_BREP_SHAPE_REPRESENTATION('',(#577),#19470);
#567=STYLED_ITEM('',(#19587),#577);
#577=MANIFOLD_SOLID_BREP('Body1',#7160);
#651=FACE_BOUND('',#1706,.T.);
#652=FACE_BOUND('',#1708,.T.);
#818=PLANE('',#7809);
#819=PLANE('',#7810);
#1225=FACE_OUTER_BOUND('',#1703,.T.);
#1226=FACE_OUTER_BOUND('',#1704,.T.);
#1227=FACE_OUTER_BOUND('',#1705,.T.);
#1228=FACE_OUTER_BOUND('',#1707,.T.);
#1703=EDGE_LOOP('',(#6589,#6590,#6591,#6592));
#1704=EDGE_LOOP('',(#6593,#6594,#6595,#6596));
#1705=EDGE_LOOP('',(#6597));
#1706=EDGE_LOOP('',(#6598));
#1707=EDGE_LOOP('',(#6599));
#1708=EDGE_LOOP('',(#6600));
#2181=LINE('',#19428,#2655);
#2182=LINE('',#19434,#2656);
#2655=VECTOR('',#9357,0.41);
#2656=VECTOR('',#9364,0.6);
#2843=CIRCLE('',#7804,0.41);
#2844=CIRCLE('',#7805,0.41);
#2845=CIRCLE('',#7807,0.6);
#2846=CIRCLE('',#7808,0.6);
#3507=VERTEX_POINT('',#19425);
#3508=VERTEX_POINT('',#19427);
#3509=VERTEX_POINT('',#19431);
#3510=VERTEX_POINT('',#19433);
#4535=EDGE_CURVE('',#3507,#3507,#2843,.T.);
#4536=EDGE_CURVE('',#3507,#3508,#2181,.T.);
#4537=EDGE_CURVE('',#3508,#3508,#2844,.T.);
#4538=EDGE_CURVE('',#3509,#3509,#2845,.T.);
#4539=EDGE_CURVE('',#3509,#3510,#2182,.T.);
#4540=EDGE_CURVE('',#3510,#3510,#2846,.T.);
#6589=ORIENTED_EDGE('',*,*,#4535,.F.);
#6590=ORIENTED_EDGE('',*,*,#4536,.T.);
#6591=ORIENTED_EDGE('',*,*,#4537,.T.);
#6592=ORIENTED_EDGE('',*,*,#4536,.F.);
#6593=ORIENTED_EDGE('',*,*,#4538,.F.);
#6594=ORIENTED_EDGE('',*,*,#4539,.T.);
#6595=ORIENTED_EDGE('',*,*,#4540,.T.);
#6596=ORIENTED_EDGE('',*,*,#4539,.F.);
#6597=ORIENTED_EDGE('',*,*,#4538,.T.);
#6598=ORIENTED_EDGE('',*,*,#4535,.T.);
#6599=ORIENTED_EDGE('',*,*,#4540,.F.);
#6600=ORIENTED_EDGE('',*,*,#4537,.F.);
#6740=CYLINDRICAL_SURFACE('',#7803,0.41);
#6741=CYLINDRICAL_SURFACE('',#7806,0.6);
#7147=ADVANCED_FACE('',(#1225),#6740,.F.);
#7148=ADVANCED_FACE('',(#1226),#6741,.T.);
#7149=ADVANCED_FACE('',(#1227,#651),#818,.T.);
#7150=ADVANCED_FACE('',(#1228,#652),#819,.F.);
#7160=CLOSED_SHELL('',(#7147,#7148,#7149,#7150));
#7802=AXIS2_PLACEMENT_3D('',#19423,#9351,#9352);
#7803=AXIS2_PLACEMENT_3D('',#19424,#9353,#9354);
#7804=AXIS2_PLACEMENT_3D('',#19426,#9355,#9356);
#7805=AXIS2_PLACEMENT_3D('',#19429,#9358,#9359);
#7806=AXIS2_PLACEMENT_3D('',#19430,#9360,#9361);
#7807=AXIS2_PLACEMENT_3D('',#19432,#9362,#9363);
#7808=AXIS2_PLACEMENT_3D('',#19435,#9365,#9366);
#7809=AXIS2_PLACEMENT_3D('',#19436,#9367,#9368);
#7810=AXIS2_PLACEMENT_3D('',#19437,#9369,#9370);
#9351=DIRECTION('axis',(0.,0.,1.));
#9352=DIRECTION('refdir',(1.,0.,0.));
#9353=DIRECTION('center_axis',(0.,0.,1.));
#9354=DIRECTION('ref_axis',(1.,0.,0.));
#9355=DIRECTION('center_axis',(0.,0.,-1.));
#9356=DIRECTION('ref_axis',(1.,0.,0.));
#9357=DIRECTION('',(0.,0.,-1.));
#9358=DIRECTION('center_axis',(0.,0.,-1.));
#9359=DIRECTION('ref_axis',(1.,0.,0.));
#9360=DIRECTION('center_axis',(0.,0.,1.));
#9361=DIRECTION('ref_axis',(1.,0.,0.));
#9362=DIRECTION('center_axis',(0.,0.,1.));
#9363=DIRECTION('ref_axis',(1.,0.,0.));
#9364=DIRECTION('',(0.,0.,-1.));
#9365=DIRECTION('center_axis',(0.,0.,1.));
#9366=DIRECTION('ref_axis',(1.,0.,0.));
#9367=DIRECTION('center_axis',(0.,0.,1.));
#9368=DIRECTION('ref_axis',(1.,0.,0.));
#9369=DIRECTION('center_axis',(0.,0.,1.));
#9370=DIRECTION('ref_axis',(1.,0.,0.));
#19423=CARTESIAN_POINT('',(0.,0.,0.));
#19424=CARTESIAN_POINT('Origin',(0.,0.,0.));
#19425=CARTESIAN_POINT('',(-0.41,-5.02105187650415E-17,0.1));
#19426=CARTESIAN_POINT('Origin',(0.,0.,0.1));
#19427=CARTESIAN_POINT('',(-0.41,-5.02105187650415E-17,0.));
#19428=CARTESIAN_POINT('',(-0.41,-5.02105187650415E-17,0.));
#19429=CARTESIAN_POINT('Origin',(0.,0.,0.));
#19430=CARTESIAN_POINT('Origin',(0.,0.,0.));
#19431=CARTESIAN_POINT('',(-0.6,-7.34788079488412E-17,0.1));
#19432=CARTESIAN_POINT('Origin',(0.,0.,0.1));
#19433=CARTESIAN_POINT('',(-0.6,-7.34788079488412E-17,0.));
#19434=CARTESIAN_POINT('',(-0.6,-7.34788079488412E-17,0.));
#19435=CARTESIAN_POINT('Origin',(0.,0.,0.));
#19436=CARTESIAN_POINT('Origin',(0.,0.,0.1));
#19437=CARTESIAN_POINT('Origin',(0.,0.,0.));
#19457=UNCERTAINTY_MEASURE_WITH_UNIT(LENGTH_MEASURE(0.001),#19472,
'DISTANCE_ACCURACY_VALUE',
'Maximum model space distance between geometric entities at asserted c
onnectivities');
#19458=UNCERTAINTY_MEASURE_WITH_UNIT(LENGTH_MEASURE(0.001),#19472,
'DISTANCE_ACCURACY_VALUE',
'Maximum model space distance between geometric entities at asserted c
onnectivities');
#19470=(
GEOMETRIC_REPRESENTATION_CONTEXT(3)
GLOBAL_UNCERTAINTY_ASSIGNED_CONTEXT((#19457))
GLOBAL_UNIT_ASSIGNED_CONTEXT((#19472,#19474,#19475))
REPRESENTATION_CONTEXT('','3D')
);
#19471=(
GEOMETRIC_REPRESENTATION_CONTEXT(3)
GLOBAL_UNCERTAINTY_ASSIGNED_CONTEXT((#19458))
GLOBAL_UNIT_ASSIGNED_CONTEXT((#19472,#19474,#19475))
REPRESENTATION_CONTEXT('','3D')
);
#19472=(
LENGTH_UNIT()
NAMED_UNIT(*)
SI_UNIT(.CENTI.,.METRE.)
);
#19474=(
NAMED_UNIT(*)
PLANE_ANGLE_UNIT()
SI_UNIT($,.RADIAN.)
);
#19475=(
NAMED_UNIT(*)
SI_UNIT($,.STERADIAN.)
SOLID_ANGLE_UNIT()
);
#19487=SHAPE_DEFINITION_REPRESENTATION(#19507,#19527);
#19507=PRODUCT_DEFINITION_SHAPE('',$,#19540);
#19527=SHAPE_REPRESENTATION('',(#7802),#19470);
#19528=PRODUCT_DEFINITION_CONTEXT('part definition',#19566,'design');
#19540=PRODUCT_DEFINITION('Pivot thrust washer','Pivot thrust washer',#19552,
#19528);
#19552=PRODUCT_DEFINITION_FORMATION('',$,#19579);
#19566=APPLICATION_CONTEXT(
'Core Data for Automotive Mechanical Design Process');
#19567=PRODUCT_CONTEXT('part definition',#19566,'mechanical');
#19579=PRODUCT('Pivot thrust washer','Pivot thrust washer',$,(#19567));
#19587=PRESENTATION_STYLE_ASSIGNMENT((#19595));
#19595=SURFACE_STYLE_USAGE(.BOTH.,#19603);
#19603=SURFACE_SIDE_STYLE('',(#19611));
#19611=SURFACE_STYLE_FILL_AREA(#19619);
#19619=FILL_AREA_STYLE('Washer gray',(#19627));
#19627=FILL_AREA_STYLE_COLOUR('Washer gray',#19635);
#19635=COLOUR_RGB('Washer gray',0.725490196078431,0.752941176470588,0.792156862745098);
ENDSEC;
END-ISO-10303-21;
